ISO-10303-21;
HEADER;
/* Generated by software containing ST-Developer
 * from STEP Tools, Inc. (www.steptools.com) 
 */

FILE_DESCRIPTION(
/* description */ ('Chain-less indexing wheel (Geneva) drive'),
/* implementation_level */ '2;1');

FILE_NAME(
/* name */ 'M4x10 Cap Screw.step',
/* time_stamp */ '2026-10-28T03:25:22-07:00',
/* author */ (''),
/* organization */ (''),
/* preprocessor_version */ 'ST-DEVELOPER v20.2',
/* originating_system */ 'Autodesk Translation Framework v15.17.0.0',
/* authorisation */ '');

FILE_SCHEMA (('AUTOMOTIVE_DESIGN { 1 0 10303 214 3 1 1 }'));
ENDSEC;

DATA;
#10=MECHANICAL_DESIGN_GEOMETRIC_PRESENTATION_REPRESENTATION('',(#331),#10957);
#198=ORIENTED_CLOSED_SHELL('',*,#5728,.F.);
#207=CONICAL_SURFACE('',#6538,0.325,0.785398163397448);
#208=CONICAL_SURFACE('',#6542,0.335,0.785398163397448);
#209=CONICAL_SURFACE('',#6546,0.21,0.463647609000806);
#212=BREP_WITH_VOIDS('Body1',#5729,(#198));
#273=SHAPE_REPRESENTATION_RELATIONSHIP('SRR','None',#11088,#298);
#298=ADVANCED_BREP_SHAPE_REPRESENTATION('',(#212),#10951);
#331=STYLED_ITEM('',(#11294),#212);
#455=FACE_BOUND('',#1322,.T.);
#589=PLANE('',#6526);
#590=PLANE('',#6527);
#591=PLANE('',#6528);
#592=PLANE('',#6529);
#593=PLANE('',#6530);
#594=PLANE('',#6531);
#595=PLANE('',#6532);
#596=PLANE('',#6533);
#597=PLANE('',#6534);
#598=PLANE('',#6536);
#599=PLANE('',#6544);
#887=FACE_OUTER_BOUND('',#1308,.T.);
#888=FACE_OUTER_BOUND('',#1309,.T.);
#889=FACE_OUTER_BOUND('',#1310,.T.);
#890=FACE_OUTER_BOUND('',#1311,.T.);
#891=FACE_OUTER_BOUND('',#1312,.T.);
#892=FACE_OUTER_BOUND('',#1313,.T.);
#893=FACE_OUTER_BOUND('',#1314,.T.);
#894=FACE_OUTER_BOUND('',#1315,.T.);
#895=FACE_OUTER_BOUND('',#1316,.T.);
#896=FACE_OUTER_BOUND('',#1317,.T.);
#897=FACE_OUTER_BOUND('',#1318,.T.);
#898=FACE_OUTER_BOUND('',#1319,.T.);
#899=FACE_OUTER_BOUND('',#1320,.T.);
#900=FACE_OUTER_BOUND('',#1321,.T.);
#901=FACE_OUTER_BOUND('',#1323,.T.);
#902=FACE_OUTER_BOUND('',#1324,.T.);
#1308=EDGE_LOOP('',(#4743,#4744,#4745,#4746));
#1309=EDGE_LOOP('',(#4747,#4748,#4749,#4750));
#1310=EDGE_LOOP('',(#4751,#4752,#4753,#4754));
#1311=EDGE_LOOP('',(#4755,#4756,#4757,#4758));
#1312=EDGE_LOOP('',(#4759,#4760,#4761,#4762));
#1313=EDGE_LOOP('',(#4763,#4764,#4765,#4766));
#1314=EDGE_LOOP('',(#4767,#4768,#4769,#4770,#4771,#4772));
#1315=EDGE_LOOP('',(#4773,#4774,#4775,#4776,#4777,#4778));
#1316=EDGE_LOOP('',(#4779));
#1317=EDGE_LOOP('',(#4780));
#1318=EDGE_LOOP('',(#4781,#4782,#4783,#4784));
#1319=EDGE_LOOP('',(#4785,#4786,#4787,#4788));
#1320=EDGE_LOOP('',(#4789,#4790,#4791,#4792));
#1321=EDGE_LOOP('',(#4793));
#1322=EDGE_LOOP('',(#4794));
#1323=EDGE_LOOP('',(#4795,#4796,#4797,#4798));
#1324=EDGE_LOOP('',(#4799,#4800,#4801,#4802));
#1640=LINE('',#10222,#2014);
#1641=LINE('',#10224,#2015);
#1642=LINE('',#10226,#2016);
#1643=LINE('',#10227,#2017);
#1644=LINE('',#10230,#2018);
#1645=LINE('',#10232,#2019);
#1646=LINE('',#10233,#2020);
#1647=LINE('',#10236,#2021);
#1648=LINE('',#10238,#2022);
#1649=LINE('',#10239,#2023);
#1650=LINE('',#10242,#2024);
#1651=LINE('',#10244,#2025);
#1652=LINE('',#10245,#2026);
#1653=LINE('',#10248,#2027);
#1654=LINE('',#10250,#2028);
#1655=LINE('',#10251,#2029);
#1656=LINE('',#10253,#2030);
#1657=LINE('',#10254,#2031);
#1658=LINE('',#10266,#2032);
#1659=LINE('',#10270,#2033);
#1660=LINE('',#10274,#2034);
#1661=LINE('',#10281,#2035);
#1662=LINE('',#10283,#2036);
#2014=VECTOR('',#8000,1.);
#2015=VECTOR('',#8001,1.);
#2016=VECTOR('',#8002,1.);
#2017=VECTOR('',#8003,1.);
#2018=VECTOR('',#8006,1.);
#2019=VECTOR('',#8007,1.);
#2020=VECTOR('',#8008,1.);
#2021=VECTOR('',#8011,1.);
#2022=VECTOR('',#8012,1.);
#2023=VECTOR('',#8013,1.);
#2024=VECTOR('',#8016,1.);
#2025=VECTOR('',#8017,1.);
#2026=VECTOR('',#8018,1.);
#2027=VECTOR('',#8021,1.);
#2028=VECTOR('',#8022,1.);
#2029=VECTOR('',#8023,1.);
#2030=VECTOR('',#8026,1.);
#2031=VECTOR('',#8027,1.);
#2032=VECTOR('',#8044,0.325);
#2033=VECTOR('',#8049,0.35);
#2034=VECTOR('',#8054,0.335);
#2035=VECTOR('',#8063,0.21);
#2036=VECTOR('',#8066,0.2);
#2422=CIRCLE('',#6535,0.1954);
#2423=CIRCLE('',#6537,0.3);
#2424=CIRCLE('',#6539,0.35);
#2425=CIRCLE('',#6541,0.35);
#2426=CIRCLE('',#6543,0.32);
#2427=CIRCLE('',#6545,0.22);
#2428=CIRCLE('',#6547,0.1954);
#2834=VERTEX_POINT('',#10220);
#2835=VERTEX_POINT('',#10221);
#2836=VERTEX_POINT('',#10223);
#2837=VERTEX_POINT('',#10225);
#2838=VERTEX_POINT('',#10229);
#2839=VERTEX_POINT('',#10231);
#2840=VERTEX_POINT('',#10235);
#2841=VERTEX_POINT('',#10237);
#2842=VERTEX_POINT('',#10241);
#2843=VERTEX_POINT('',#10243);
#2844=VERTEX_POINT('',#10247);
#2845=VERTEX_POINT('',#10249);
#2846=VERTEX_POINT('',#10258);
#2847=VERTEX_POINT('',#10261);
#2848=VERTEX_POINT('',#10264);
#2849=VERTEX_POINT('',#10268);
#2850=VERTEX_POINT('',#10272);
#2851=VERTEX_POINT('',#10276);
#2852=VERTEX_POINT('',#10279);
#3497=EDGE_CURVE('',#2834,#2835,#1640,.T.);
#3498=EDGE_CURVE('',#2835,#2836,#1641,.T.);
#3499=EDGE_CURVE('',#2836,#2837,#1642,.T.);
#3500=EDGE_CURVE('',#2834,#2837,#1643,.T.);
#3501=EDGE_CURVE('',#2835,#2838,#1644,.T.);
#3502=EDGE_CURVE('',#2838,#2839,#1645,.T.);
#3503=EDGE_CURVE('',#2839,#2836,#1646,.T.);
#3504=EDGE_CURVE('',#2838,#2840,#1647,.T.);
#3505=EDGE_CURVE('',#2840,#2841,#1648,.T.);
#3506=EDGE_CURVE('',#2841,#2839,#1649,.T.);
#3507=EDGE_CURVE('',#2840,#2842,#1650,.T.);
#3508=EDGE_CURVE('',#2842,#2843,#1651,.T.);
#3509=EDGE_CURVE('',#2843,#2841,#1652,.T.);
#3510=EDGE_CURVE('',#2842,#2844,#1653,.T.);
#3511=EDGE_CURVE('',#2844,#2845,#1654,.T.);
#3512=EDGE_CURVE('',#2845,#2843,#1655,.T.);
#3513=EDGE_CURVE('',#2844,#2834,#1656,.T.);
#3514=EDGE_CURVE('',#2837,#2845,#1657,.T.);
#3515=EDGE_CURVE('',#2846,#2846,#2422,.T.);
#3516=EDGE_CURVE('',#2847,#2847,#2423,.T.);
#3517=EDGE_CURVE('',#2848,#2848,#2424,.T.);
#3518=EDGE_CURVE('',#2848,#2847,#1658,.T.);
#3519=EDGE_CURVE('',#2849,#2849,#2425,.T.);
#3520=EDGE_CURVE('',#2849,#2848,#1659,.T.);
#3521=EDGE_CURVE('',#2850,#2850,#2426,.T.);
#3522=EDGE_CURVE('',#2850,#2849,#1660,.T.);
#3523=EDGE_CURVE('',#2851,#2851,#2427,.T.);
#3524=EDGE_CURVE('',#2852,#2852,#2428,.F.);
#3525=EDGE_CURVE('',#2852,#2851,#1661,.T.);
#3526=EDGE_CURVE('',#2846,#2852,#1662,.T.);
#4743=ORIENTED_EDGE('',*,*,#3497,.T.);
#4744=ORIENTED_EDGE('',*,*,#3498,.T.);
#4745=ORIENTED_EDGE('',*,*,#3499,.T.);
#4746=ORIENTED_EDGE('',*,*,#3500,.F.);
#4747=ORIENTED_EDGE('',*,*,#3501,.T.);
#4748=ORIENTED_EDGE('',*,*,#3502,.T.);
#4749=ORIENTED_EDGE('',*,*,#3503,.T.);
#4750=ORIENTED_EDGE('',*,*,#3498,.F.);
#4751=ORIENTED_EDGE('',*,*,#3504,.T.);
#4752=ORIENTED_EDGE('',*,*,#3505,.T.);
#4753=ORIENTED_EDGE('',*,*,#3506,.T.);
#4754=ORIENTED_EDGE('',*,*,#3502,.F.);
#4755=ORIENTED_EDGE('',*,*,#3507,.T.);
#4756=ORIENTED_EDGE('',*,*,#3508,.T.);
#4757=ORIENTED_EDGE('',*,*,#3509,.T.);
#4758=ORIENTED_EDGE('',*,*,#3505,.F.);
#4759=ORIENTED_EDGE('',*,*,#3510,.T.);
#4760=ORIENTED_EDGE('',*,*,#3511,.T.);
#4761=ORIENTED_EDGE('',*,*,#3512,.T.);
#4762=ORIENTED_EDGE('',*,*,#3508,.F.);
#4763=ORIENTED_EDGE('',*,*,#3513,.T.);
#4764=ORIENTED_EDGE('',*,*,#3500,.T.);
#4765=ORIENTED_EDGE('',*,*,#3514,.T.);
#4766=ORIENTED_EDGE('',*,*,#3511,.F.);
#4767=ORIENTED_EDGE('',*,*,#3513,.F.);
#4768=ORIENTED_EDGE('',*,*,#3510,.F.);
#4769=ORIENTED_EDGE('',*,*,#3507,.F.);
#4770=ORIENTED_EDGE('',*,*,#3504,.F.);
#4771=ORIENTED_EDGE('',*,*,#3501,.F.);
#4772=ORIENTED_EDGE('',*,*,#3497,.F.);
#4773=ORIENTED_EDGE('',*,*,#3514,.F.);
#4774=ORIENTED_EDGE('',*,*,#3499,.F.);
#4775=ORIENTED_EDGE('',*,*,#3503,.F.);
#4776=ORIENTED_EDGE('',*,*,#3506,.F.);
#4777=ORIENTED_EDGE('',*,*,#3509,.F.);
#4778=ORIENTED_EDGE('',*,*,#3512,.F.);
#4779=ORIENTED_EDGE('',*,*,#3515,.F.);
#4780=ORIENTED_EDGE('',*,*,#3516,.F.);
#4781=ORIENTED_EDGE('',*,*,#3517,.F.);
#4782=ORIENTED_EDGE('',*,*,#3518,.T.);
#4783=ORIENTED_EDGE('',*,*,#3516,.T.);
#4784=ORIENTED_EDGE('',*,*,#3518,.F.);
#4785=ORIENTED_EDGE('',*,*,#3519,.F.);
#4786=ORIENTED_EDGE('',*,*,#3520,.T.);
#4787=ORIENTED_EDGE('',*,*,#3517,.T.);
#4788=ORIENTED_EDGE('',*,*,#3520,.F.);
#4789=ORIENTED_EDGE('',*,*,#3521,.F.);
#4790=ORIENTED_EDGE('',*,*,#3522,.T.);
#4791=ORIENTED_EDGE('',*,*,#3519,.T.);
#4792=ORIENTED_EDGE('',*,*,#3522,.F.);
#4793=ORIENTED_EDGE('',*,*,#3521,.T.);
#4794=ORIENTED_EDGE('',*,*,#3523,.F.);
#4795=ORIENTED_EDGE('',*,*,#3524,.F.);
#4796=ORIENTED_EDGE('',*,*,#3525,.T.);
#4797=ORIENTED_EDGE('',*,*,#3523,.T.);
#4798=ORIENTED_EDGE('',*,*,#3525,.F.);
#4799=ORIENTED_EDGE('',*,*,#3515,.T.);
#4800=ORIENTED_EDGE('',*,*,#3526,.T.);
#4801=ORIENTED_EDGE('',*,*,#3524,.T.);
#4802=ORIENTED_EDGE('',*,*,#3526,.F.);
#5335=CYLINDRICAL_SURFACE('',#6540,0.35);
#5336=CYLINDRICAL_SURFACE('',#6548,0.1954);
#5601=ADVANCED_FACE('',(#887),#589,.F.);
#5602=ADVANCED_FACE('',(#888),#590,.F.);
#5603=ADVANCED_FACE('',(#889),#591,.F.);
#5604=ADVANCED_FACE('',(#890),#592,.F.);
#5605=ADVANCED_FACE('',(#891),#593,.F.);
#5606=ADVANCED_FACE('',(#892),#594,.F.);
#5607=ADVANCED_FACE('',(#893),#595,.F.);
#5608=ADVANCED_FACE('',(#894),#596,.F.);
#5609=ADVANCED_FACE('',(#895),#597,.F.);
#5610=ADVANCED_FACE('',(#896),#598,.T.);
#5611=ADVANCED_FACE('',(#897),#207,.T.);
#5612=ADVANCED_FACE('',(#898),#5335,.T.);
#5613=ADVANCED_FACE('',(#899),#208,.T.);
#5614=ADVANCED_FACE('',(#900,#455),#599,.T.);
#5615=ADVANCED_FACE('',(#901),#209,.T.);
#5616=ADVANCED_FACE('',(#902),#5336,.T.);
#5728=CLOSED_SHELL('',(#5601,#5602,#5603,#5604,#5605,#5606,#5607,#5608));
#5729=CLOSED_SHELL('',(#5609,#5610,#5611,#5612,#5613,#5614,#5615,#5616));
#6525=AXIS2_PLACEMENT_3D('',#10218,#7996,#7997);
#6526=AXIS2_PLACEMENT_3D('',#10219,#7998,#7999);
#6527=AXIS2_PLACEMENT_3D('',#10228,#8004,#8005);
#6528=AXIS2_PLACEMENT_3D('',#10234,#8009,#8010);
#6529=AXIS2_PLACEMENT_3D('',#10240,#8014,#8015);
#6530=AXIS2_PLACEMENT_3D('',#10246,#8019,#8020);
#6531=AXIS2_PLACEMENT_3D('',#10252,#8024,#8025);
#6532=AXIS2_PLACEMENT_3D('',#10255,#8028,#8029);
#6533=AXIS2_PLACEMENT_3D('',#10256,#8030,#8031);
#6534=AXIS2_PLACEMENT_3D('',#10257,#8032,#8033);
#6535=AXIS2_PLACEMENT_3D('',#10259,#8034,#8035);
#6536=AXIS2_PLACEMENT_3D('',#10260,#8036,#8037);
#6537=AXIS2_PLACEMENT_3D('',#10262,#8038,#8039);
#6538=AXIS2_PLACEMENT_3D('',#10263,#8040,#8041);
#6539=AXIS2_PLACEMENT_3D('',#10265,#8042,#8043);
#6540=AXIS2_PLACEMENT_3D('',#10267,#8045,#8046);
#6541=AXIS2_PLACEMENT_3D('',#10269,#8047,#8048);
#6542=AXIS2_PLACEMENT_3D('',#10271,#8050,#8051);
#6543=AXIS2_PLACEMENT_3D('',#10273,#8052,#8053);
#6544=AXIS2_PLACEMENT_3D('',#10275,#8055,#8056);
#6545=AXIS2_PLACEMENT_3D('',#10277,#8057,#8058);
#6546=AXIS2_PLACEMENT_3D('',#10278,#8059,#8060);
#6547=AXIS2_PLACEMENT_3D('',#10280,#8061,#8062);
#6548=AXIS2_PLACEMENT_3D('',#10282,#8064,#8065);
#7996=DIRECTION('axis',(0.,0.,1.));
#7997=DIRECTION('refdir',(1.,0.,0.));
#7998=DIRECTION('center_axis',(0.866025403784439,0.,-0.5));
#7999=DIRECTION('ref_axis',(0.5,0.,0.866025403784439));
#8000=DIRECTION('',(-0.5,0.,-0.866025403784439));
#8001=DIRECTION('',(0.,-1.,0.));
#8002=DIRECTION('',(0.5,0.,0.866025403784439));
#8003=DIRECTION('',(0.,-1.,0.));
#8004=DIRECTION('center_axis',(1.60246890531964E-16,0.,-1.));
#8005=DIRECTION('ref_axis',(1.,0.,1.60246890531964E-16));
#8006=DIRECTION('',(-1.,0.,-1.60246890531964E-16));
#8007=DIRECTION('',(0.,-1.,0.));
#8008=DIRECTION('',(1.,0.,1.60246890531964E-16));
#8009=DIRECTION('center_axis',(-0.866025403784439,0.,-0.5));
#8010=DIRECTION('ref_axis',(0.5,0.,-0.866025403784439));
#8011=DIRECTION('',(-0.5,0.,0.866025403784439));
#8012=DIRECTION('',(0.,-1.,0.));
#8013=DIRECTION('',(0.5,0.,-0.866025403784439));
#8014=DIRECTION('center_axis',(-0.866025403784439,0.,0.5));
#8015=DIRECTION('ref_axis',(-0.5,0.,-0.866025403784439));
#8016=DIRECTION('',(0.5,0.,0.866025403784439));
#8017=DIRECTION('',(0.,-1.,0.));
#8018=DIRECTION('',(-0.5,0.,-0.866025403784439));
#8019=DIRECTION('center_axis',(-1.60246890531964E-16,0.,1.));
#8020=DIRECTION('ref_axis',(-1.,0.,-1.60246890531964E-16));
#8021=DIRECTION('',(1.,0.,1.60246890531964E-16));
#8022=DIRECTION('',(0.,-1.,0.));
#8023=DIRECTION('',(-1.,0.,-1.60246890531964E-16));
#8024=DIRECTION('center_axis',(0.866025403784439,0.,0.5));
#8025=DIRECTION('ref_axis',(-0.5,0.,0.866025403784439));
#8026=DIRECTION('',(0.5,0.,-0.866025403784439));
#8027=DIRECTION('',(-0.5,0.,0.866025403784439));
#8028=DIRECTION('center_axis',(0.,1.,0.));
#8029=DIRECTION('ref_axis',(1.,0.,0.));
#8030=DIRECTION('center_axis',(0.,-1.,0.));
#8031=DIRECTION('ref_axis',(0.,0.,-1.));
#8032=DIRECTION('center_axis',(0.,1.,0.));
#8033=DIRECTION('ref_axis',(1.,0.,0.));
#8034=DIRECTION('center_axis',(0.,1.,0.));
#8035=DIRECTION('ref_axis',(1.,0.,0.));
#8036=DIRECTION('center_axis',(0.,1.,0.));
#8037=DIRECTION('ref_axis',(0.,0.,1.));
#8038=DIRECTION('center_axis',(0.,-1.,0.));
#8039=DIRECTION('ref_axis',(1.,0.,0.));
#8040=DIRECTION('center_axis',(0.,-1.,0.));
#8041=DIRECTION('ref_axis',(1.,0.,0.));
#8042=DIRECTION('center_axis',(0.,-1.,0.));
#8043=DIRECTION('ref_axis',(1.,0.,0.));
#8044=DIRECTION('',(0.707106781186547,0.707106781186548,8.65956056235493E-17));
#8045=DIRECTION('center_axis',(0.,-1.,0.));
#8046=DIRECTION('ref_axis',(1.,0.,0.));
#8047=DIRECTION('center_axis',(0.,-1.,0.));
#8048=DIRECTION('ref_axis',(1.,0.,0.));
#8049=DIRECTION('',(0.,1.,0.));
#8050=DIRECTION('center_axis',(0.,1.,0.));
#8051=DIRECTION('ref_axis',(1.,0.,0.));
#8052=DIRECTION('center_axis',(0.,-1.,0.));
#8053=DIRECTION('ref_axis',(1.,0.,0.));
#8054=DIRECTION('',(-0.707106781186547,0.707106781186548,-8.65956056235493E-17));
#8055=DIRECTION('center_axis',(0.,-1.,0.));
#8056=DIRECTION('ref_axis',(0.,0.,-1.));
#8057=DIRECTION('center_axis',(0.,-1.,0.));
#8058=DIRECTION('ref_axis',(1.,0.,0.));
#8059=DIRECTION('center_axis',(0.,1.,0.));
#8060=DIRECTION('ref_axis',(1.,0.,0.));
#8061=DIRECTION('center_axis',(0.,1.,0.));
#8062=DIRECTION('ref_axis',(1.,0.,0.));
#8063=DIRECTION('',(-0.447213595499958,0.894427190999916,-5.47678698264203E-17));
#8064=DIRECTION('center_axis',(0.,-1.,0.));
#8065=DIRECTION('ref_axis',(1.,0.,0.));
#8066=DIRECTION('',(0.,1.,0.));
#10218=CARTESIAN_POINT('',(0.,0.,0.));
#10219=CARTESIAN_POINT('Origin',(0.0866025403784439,-0.4,-0.15));
#10220=CARTESIAN_POINT('',(0.173205080756888,-0.4,0.));
#10221=CARTESIAN_POINT('',(0.0866025403784439,-0.4,-0.15));
#10222=CARTESIAN_POINT('',(0.173205080756888,-0.4,0.));
#10223=CARTESIAN_POINT('',(0.0866025403784439,-0.64,-0.15));
#10224=CARTESIAN_POINT('',(0.0866025403784439,-0.4,-0.15));
#10225=CARTESIAN_POINT('',(0.173205080756888,-0.64,0.));
#10226=CARTESIAN_POINT('',(0.173205080756888,-0.64,0.));
#10227=CARTESIAN_POINT('',(0.173205080756888,-0.4,0.));
#10228=CARTESIAN_POINT('Origin',(-0.0866025403784438,-0.4,-0.15));
#10229=CARTESIAN_POINT('',(-0.0866025403784438,-0.4,-0.15));
#10230=CARTESIAN_POINT('',(0.0866025403784439,-0.4,-0.15));
#10231=CARTESIAN_POINT('',(-0.0866025403784438,-0.64,-0.15));
#10232=CARTESIAN_POINT('',(-0.0866025403784438,-0.4,-0.15));
#10233=CARTESIAN_POINT('',(0.0866025403784439,-0.64,-0.15));
#10234=CARTESIAN_POINT('Origin',(-0.173205080756888,-0.4,-2.77555756156289E-17));
#10235=CARTESIAN_POINT('',(-0.173205080756888,-0.4,-2.12115047744981E-17));
#10236=CARTESIAN_POINT('',(-0.0866025403784438,-0.4,-0.15));
#10237=CARTESIAN_POINT('',(-0.173205080756888,-0.64,-2.77555756156289E-17));
#10238=CARTESIAN_POINT('',(-0.173205080756888,-0.4,-2.12115047744981E-17));
#10239=CARTESIAN_POINT('',(-0.0866025403784438,-0.64,-0.15));
#10240=CARTESIAN_POINT('Origin',(-0.0866025403784439,-0.4,0.15));
#10241=CARTESIAN_POINT('',(-0.0866025403784439,-0.4,0.15));
#10242=CARTESIAN_POINT('',(-0.173205080756888,-0.4,-2.12115047744981E-17));
#10243=CARTESIAN_POINT('',(-0.0866025403784439,-0.64,0.15));
#10244=CARTESIAN_POINT('',(-0.0866025403784439,-0.4,0.15));
#10245=CARTESIAN_POINT('',(-0.173205080756888,-0.64,-2.12115047744981E-17));
#10246=CARTESIAN_POINT('Origin',(0.0866025403784439,-0.4,0.15));
#10247=CARTESIAN_POINT('',(0.0866025403784439,-0.4,0.15));
#10248=CARTESIAN_POINT('',(-0.0866025403784439,-0.4,0.15));
#10249=CARTESIAN_POINT('',(0.0866025403784439,-0.64,0.15));
#10250=CARTESIAN_POINT('',(0.0866025403784439,-0.4,0.15));
#10251=CARTESIAN_POINT('',(-0.0866025403784439,-0.64,0.15));
#10252=CARTESIAN_POINT('Origin',(0.173205080756888,-0.4,0.));
#10253=CARTESIAN_POINT('',(0.0866025403784439,-0.4,0.15));
#10254=CARTESIAN_POINT('',(0.0866025403784439,-0.64,0.15));
#10255=CARTESIAN_POINT('Origin',(0.,-0.4,-2.77555756156289E-17));
#10256=CARTESIAN_POINT('Origin',(0.,-0.64,-2.77555756156289E-17));
#10257=CARTESIAN_POINT('Origin',(0.,-1.,0.));
#10258=CARTESIAN_POINT('',(-0.1954,-1.,2.39295984553393E-17));
#10259=CARTESIAN_POINT('Origin',(0.,-1.,0.));
#10260=CARTESIAN_POINT('Origin',(0.3,0.4,0.));
#10261=CARTESIAN_POINT('',(-0.3,0.4,-3.67394039744206E-17));
#10262=CARTESIAN_POINT('Origin',(0.,0.4,0.));
#10263=CARTESIAN_POINT('Origin',(0.,0.375,0.));
#10264=CARTESIAN_POINT('',(-0.35,0.35,-4.28626379701573E-17));
#10265=CARTESIAN_POINT('Origin',(0.,0.35,0.));
#10266=CARTESIAN_POINT('',(-0.325,0.375,-3.9801020972289E-17));
#10267=CARTESIAN_POINT('Origin',(0.,0.19,0.));
#10268=CARTESIAN_POINT('',(-0.35,0.03,-4.28626379701574E-17));
#10269=CARTESIAN_POINT('Origin',(0.,0.03,0.));
#10270=CARTESIAN_POINT('',(-0.35,0.19,-4.28626379701574E-17));
#10271=CARTESIAN_POINT('Origin',(0.,0.0149999999999999,0.));
#10272=CARTESIAN_POINT('',(-0.32,-3.29597460435593E-17,-3.91886975727153E-17));
#10273=CARTESIAN_POINT('Origin',(0.,0.,0.));
#10274=CARTESIAN_POINT('',(-0.335,0.0149999999999999,-4.10256677714363E-17));
#10275=CARTESIAN_POINT('Origin',(0.22,0.,0.));
#10276=CARTESIAN_POINT('',(-0.22,-6.93889390390723E-18,-2.69422295812418E-17));
#10277=CARTESIAN_POINT('Origin',(0.,0.,0.));
#10278=CARTESIAN_POINT('Origin',(0.,-0.02,0.));
#10279=CARTESIAN_POINT('',(-0.1954,-0.0492,2.39295984553393E-17));
#10280=CARTESIAN_POINT('Origin',(0.,-0.0492,0.));
#10281=CARTESIAN_POINT('',(-0.21,-0.02,-2.57175827820944E-17));
#10282=CARTESIAN_POINT('Origin',(0.,-0.8,0.));
#10283=CARTESIAN_POINT('',(-0.1954,-0.8,-2.39295984553393E-17));
#10920=UNCERTAINTY_MEASURE_WITH_UNIT(LENGTH_MEASURE(0.001),#10958,
'DISTANCE_ACCURACY_VALUE',
'Maximum model space distance between geometric entities at asserted c
onnectivities');
#10926=UNCERTAINTY_MEASURE_WITH_UNIT(LENGTH_MEASURE(0.001),#10958,
'DISTANCE_ACCURACY_VALUE',
'Maximum model space distance between geometric entities at asserted c
onnectivities');
#10951=(
GEOMETRIC_REPRESENTATION_CONTEXT(3)
GLOBAL_UNCERTAINTY_ASSIGNED_CONTEXT((#10920))
GLOBAL_UNIT_ASSIGNED_CONTEXT((#10958,#10960,#10961))
REPRESENTATION_CONTEXT('','3D')
);
#10957=(
GEOMETRIC_REPRESENTATION_CONTEXT(3)
GLOBAL_UNCERTAINTY_ASSIGNED_CONTEXT((#10926))
GLOBAL_UNIT_ASSIGNED_CONTEXT((#10958,#10960,#10961))
REPRESENTATION_CONTEXT('','3D')
);
#10958=(
LENGTH_UNIT()
NAMED_UNIT(*)
SI_UNIT(.CENTI.,.METRE.)
);
#10960=(
NAMED_UNIT(*)
PLANE_ANGLE_UNIT()
SI_UNIT($,.RADIAN.)
);
#10961=(
NAMED_UNIT(*)
SI_UNIT($,.STERADIAN.)
SOLID_ANGLE_UNIT()
);
#10986=SHAPE_DEFINITION_REPRESENTATION(#11021,#11088);
#11021=PRODUCT_DEFINITION_SHAPE('',$,#11119);
#11088=SHAPE_REPRESENTATION('',(#6525),#10951);
#11094=PRODUCT_DEFINITION_CONTEXT('part definition',#11186,'design');
#11119=PRODUCT_DEFINITION('M4x10 Cap Screw','M4x10 Cap Screw',#11149,#11094);
#11149=PRODUCT_DEFINITION_FORMATION('',$,#11212);
#11186=APPLICATION_CONTEXT(
'Core Data for Automotive Mechanical Design Process');
#11187=PRODUCT_CONTEXT('part definition',#11186,'mechanical');
#11212=PRODUCT('M4x10 Cap Screw','M4x10 Cap Screw','M4x10 Cap Screw',(#11187));
#11288=COLOUR_RGB('Black',0.12,0.14,0.17);
#11289=FILL_AREA_STYLE_COLOUR('',#11288);
#11290=FILL_AREA_STYLE('',(#11289));
#11291=SURFACE_STYLE_FILL_AREA(#11290);
#11292=SURFACE_SIDE_STYLE('',(#11291));
#11293=SURFACE_STYLE_USAGE(.BOTH.,#11292);
#11294=PRESENTATION_STYLE_ASSIGNMENT((#11293));
ENDSEC;
END-ISO-10303-21;
